ISO-10303-21;
HEADER;
FILE_DESCRIPTION (('STEP AP214'),
    '1' );
FILE_NAME ('angular contact ball bearing_68_iso_ISO 15 ABB - 1720 - 28,SI,NC,28_68.step',
    '2026-10-24T14:05:44',
    ( '' ),
    ( '' ),
    'SwSTEP 2.0',
    'SolidWorks 2026',
    '' );
FILE_SCHEMA (( 'AUTOMOTIVE_DESIGN' ));
ENDSEC;

DATA;
#2=ORIENTED_EDGE ( 'NONE', *, *, #1816, .F. ) ;
#14=ORIENTED_EDGE ( 'NONE', *, *, #3601, .F. ) ;
#26=DIRECTION ( 'NONE',  ( 1.000000000000000000, 0.000000000000000000, 0.000000000000000000 ) ) ;
#33=AXIS2_PLACEMENT_3D ( 'NONE', #4684, #4191, #721 ) ;
#46=ORIENTED_EDGE ( 'NONE', *, *, #4516, .T. ) ;
#57=FACE_OUTER_BOUND ( 'NONE', #1161, .T. ) ;
#77=AXIS2_PLACEMENT_3D ( 'NONE', #800, #3054, #1978 ) ;
#85=EDGE_LOOP ( 'NONE', ( #6499, #7166 ) ) ;
#91=CARTESIAN_POINT ( 'NONE',  ( -20.63749999999999929, 1.353234713057825478E-15, 11.05000000000000071 ) ) ;
#113=EDGE_CURVE ( 'NONE', #3854, #1142, #3125, .T. ) ;
#120=DIRECTION ( 'NONE',  ( 0.000000000000000000, 0.000000000000000000, -1.000000000000000000 ) ) ;
#132=ADVANCED_FACE ( 'NONE', ( #414, #336 ), #6742, .T. ) ;
#137=CIRCLE ( 'NONE', #621, 1.050000000000000488 ) ;
#154=TOROIDAL_SURFACE ( 'NONE', #6366, 10.20000000000000107, 0.2000000000000031197 ) ;
#159=CARTESIAN_POINT ( 'NONE',  ( -1.999999999999998224, 1.353234713057825478E-15, 11.05000000000000071 ) ) ;
#175=EDGE_CURVE ( 'NONE', #2749, #3012, #3113, .T. ) ;
#177=CIRCLE ( 'NONE', #883, 12.77500000000000036 ) ;
#187=ADVANCED_FACE ( 'NONE', ( #3805 ), #4852, .F. ) ;
#233=CARTESIAN_POINT ( 'NONE',  ( -1.800000000000002931, 0.000000000000000000, -13.50000000000000355 ) ) ;
#242=CARTESIAN_POINT ( 'NONE',  ( -0.7826237921249277196, 0.000000000000000000, -11.05000000000000071 ) ) ;
#253=DIRECTION ( 'NONE',  ( 1.000000000000000000, 0.000000000000000000, 0.000000000000000000 ) ) ;
#278=DIRECTION ( 'NONE',  ( 0.000000000000000000, 1.000000000000000000, -1.224646799147353207E-16 ) ) ;
#279=FACE_OUTER_BOUND ( 'NONE', #3322, .T. ) ;
#284=ORIENTED_EDGE ( 'NONE', *, *, #5933, .F. ) ;
#293=ORIENTED_EDGE ( 'NONE', *, *, #6948, .T. ) ;
#311=CIRCLE ( 'NONE', #2556, 12.77500000000000036 ) ;
#320=CARTESIAN_POINT ( 'NONE',  ( -2.000000000000001776, 1.641026710857453312E-15, 13.29999999999999893 ) ) ;
#324=DIRECTION ( 'NONE',  ( 0.000000000000000000, 0.000000000000000000, -1.000000000000000000 ) ) ;
#329=EDGE_CURVE ( 'NONE', #5766, #3104, #1067, .T. ) ;
#336=FACE_OUTER_BOUND ( 'NONE', #85, .T. ) ;
#345=PRODUCT_DEFINITION_SHAPE ( 'NONE', 'NONE',  #6385 ) ;
#353=CARTESIAN_POINT ( 'NONE',  ( -20.63749999999999929, 0.000000000000000000, 0.000000000000000000 ) ) ;
#358=LINE ( 'NONE', #4400, #970 ) ;
#361=EDGE_CURVE ( 'NONE', #380, #4483, #3166, .T. ) ;
#371=DIRECTION ( 'NONE',  ( -0.000000000000000000, 0.000000000000000000, 1.000000000000000000 ) ) ;
#378=ADVANCED_FACE ( 'NONE', ( #2736 ), #2063, .T. ) ;
#380=VERTEX_POINT ( 'NONE', #949 ) ;
#390=TOROIDAL_SURFACE ( 'NONE', #1109, 11.75000000000000000, 1.050000000000000266 ) ;
#395=EDGE_CURVE ( 'NONE', #3857, #5898, #757, .T. ) ;
#400=FILL_AREA_STYLE ('',( #3302 ) ) ;
#408=ORIENTED_EDGE ( 'NONE', *, *, #941, .F. ) ;
#414=FACE_BOUND ( 'NONE', #6136, .T. ) ;
#415=CARTESIAN_POINT ( 'NONE',  ( -20.63749999999999574, 0.000000000000000000, 0.000000000000000000 ) ) ;
#423=DIRECTION ( 'NONE',  ( 1.000000000000000000, 0.000000000000000000, 0.000000000000000000 ) ) ;
#437=AXIS2_PLACEMENT_3D ( 'NONE', #4317, #2581, #917 ) ;
#455=DIRECTION ( 'NONE',  ( 0.000000000000000000, 0.000000000000000000, -1.000000000000000000 ) ) ;
#478=VERTEX_POINT ( 'NONE', #320 ) ;
#482=CARTESIAN_POINT ( 'NONE',  ( -2.000000000000001776, 0.000000000000000000, -13.29999999999999893 ) ) ;
#483=( NAMED_UNIT ( * ) PLANE_ANGLE_UNIT ( ) SI_UNIT ( $, .RADIAN. ) );
#484=EDGE_CURVE ( 'NONE', #3104, #5307, #4352, .T. ) ;
#490=ORIENTED_EDGE ( 'NONE', *, *, #2940, .T. ) ;
#503=LINE ( 'NONE', #3939, #965 ) ;
#506=CARTESIAN_POINT ( 'NONE',  ( 1.800000000000002931, 0.000000000000000000, -13.50000000000000178 ) ) ;
#507=CIRCLE ( 'NONE', #5271, 12.44999999999999929 ) ;
#523=ORIENTED_EDGE ( 'NONE', *, *, #7193, .F. ) ;
#530=AXIS2_PLACEMENT_3D ( 'NONE', #1311, #5247, #5852 ) ;
#543=DIRECTION ( 'NONE',  ( 1.000000000000000000, 0.000000000000000000, 0.000000000000000000 ) ) ;
#545=DIRECTION ( 'NONE',  ( 1.000000000000000000, 0.000000000000000000, 0.000000000000000000 ) ) ;
#567=ADVANCED_FACE ( 'NONE', ( #2014 ), #1429, .T. ) ;
#577=LINE ( 'NONE', #6259, #6396 ) ;
#592=ORIENTED_EDGE ( 'NONE', *, *, #1151, .F. ) ;
#602=ADVANCED_FACE ( 'NONE', ( #279 ), #4481, .T. ) ;
#621=AXIS2_PLACEMENT_3D ( 'NONE', #5510, #4279, #4360 ) ;
#628=DIRECTION ( 'NONE',  ( 0.000000000000000000, 0.000000000000000000, 1.000000000000000000 ) ) ;
#638=EDGE_CURVE ( 'NONE', #5460, #3234, #3393, .T. ) ;
#649=CARTESIAN_POINT ( 'NONE',  ( -2.000000000000001776, 0.000000000000000000, -12.77500000000000036 ) ) ;
#657=AXIS2_PLACEMENT_3D ( 'NONE', #6929, #4215, #1855 ) ;
#673=CARTESIAN_POINT ( 'NONE',  ( 2.000000000000001776, 0.000000000000000000, 0.000000000000000000 ) ) ;
#682=MECHANICAL_DESIGN_GEOMETRIC_PRESENTATION_REPRESENTATION('',(#6426),#3527);
#700=ORIENTED_EDGE ( 'NONE', *, *, #329, .T. ) ;
#721=DIRECTION ( 'NONE',  ( 0.000000000000000000, 0.000000000000000000, -1.000000000000000000 ) ) ;
#735=EDGE_CURVE ( 'NONE', #3068, #3709, #577, .T. ) ;
#744=CYLINDRICAL_SURFACE ( 'NONE', #7079, 11.05000000000000071 ) ;
#746=EDGE_CURVE ( 'NONE', #3709, #5646, #7108, .T. ) ;
#750=ORIENTED_EDGE ( 'NONE', *, *, #175, .F. ) ;
#753=DIRECTION ( 'NONE',  ( 0.000000000000000000, 0.000000000000000000, -1.000000000000000000 ) ) ;
#757=CIRCLE ( 'NONE', #6087, 11.05000000000000071 ) ;
#770=AXIS2_PLACEMENT_3D ( 'NONE', #1738, #3448, #5781 ) ;
#774=VECTOR ( 'NONE', #4510, 1000.000000000000000 ) ;
#775=ORIENTED_EDGE ( 'NONE', *, *, #1901, .F. ) ;
#778=EDGE_CURVE ( 'NONE', #2792, #2671, #5384, .T. ) ;
#800=CARTESIAN_POINT ( 'NONE',  ( 0.000000000000000000, 1.438959988998140160E-15, -11.75000000000000000 ) ) ;
#827=ORIENTED_EDGE ( 'NONE', *, *, #4703, .F. ) ;
#833=CARTESIAN_POINT ( 'NONE',  ( 1.800000000000001155, 1.628780242865979758E-15, 13.29999999999999893 ) ) ;
#841=VERTEX_POINT ( 'NONE', #6475 ) ;
#844=AXIS2_PLACEMENT_3D ( 'NONE', #3298, #2542, #6009 ) ;
#845=CARTESIAN_POINT ( 'NONE',  ( 1.799999999999996048, 0.000000000000000000, -10.20000000000000107 ) ) ;
#855=CIRCLE ( 'NONE', #6733, 12.44999999999999929 ) ;
#856=MANIFOLD_SOLID_BREP ( 'OuterRace', #1716 ) ;
#865=ADVANCED_FACE ( 'NONE', ( #4376 ), #2371, .F. ) ;
#870=PRODUCT ( 'angular contact ball bearing_68_iso_ISO 15 ABB - 1720 - 28,SI,NC,28_68', 'angular contact ball bearing_68_iso_ISO 15 ABB - 1720 - 28,SI,NC,28_68', '', ( #4556 ) ) ;
#883=AXIS2_PLACEMENT_3D ( 'NONE', #6871, #1692, #6315 ) ;
#887=TOROIDAL_SURFACE ( 'NONE', #3398, 10.20000000000000107, 0.2000000000000031197 ) ;
#889=CARTESIAN_POINT ( 'NONE',  ( -20.63749999999999574, 0.000000000000000000, 0.000000000000000000 ) ) ;
#896=FACE_OUTER_BOUND ( 'NONE', #1807, .T. ) ;
#917=DIRECTION ( 'NONE',  ( 0.000000000000000000, 0.000000000000000000, -1.000000000000000000 ) ) ;
#918=VERTEX_POINT ( 'NONE', #1997 ) ;
#923=CARTESIAN_POINT ( 'NONE',  ( -2.000000000000001776, 1.564486285910744042E-15, 12.77500000000000213 ) ) ;
#935=DIRECTION ( 'NONE',  ( 0.000000000000000000, 0.000000000000000000, -1.000000000000000000 ) ) ;
#941=EDGE_CURVE ( 'NONE', #5766, #918, #1514, .T. ) ;
#943=EDGE_LOOP ( 'NONE', ( #7044, #3226 ) ) ;
#949=CARTESIAN_POINT ( 'NONE',  ( 0.7826237921249276086, 1.524685264938454646E-15, -12.44999999999999929 ) ) ;
#959=DIRECTION ( 'NONE',  ( 1.000000000000000000, 0.000000000000000000, 0.000000000000000000 ) ) ;
#965=VECTOR ( 'NONE', #5168, 1000.000000000000000 ) ;
#970=VECTOR ( 'NONE', #3753, 1000.000000000000000 ) ;
#971=FACE_OUTER_BOUND ( 'NONE', #6440, .T. ) ;
#983=CARTESIAN_POINT ( 'NONE',  ( -1.800000000000002931, 0.000000000000000000, 0.000000000000000000 ) ) ;
#992=AXIS2_PLACEMENT_3D ( 'NONE', #1897, #6975, #4193 ) ;
#1005=FACE_OUTER_BOUND ( 'NONE', #5871, .T. ) ;
#1032=DIRECTION ( 'NONE',  ( 1.000000000000000000, 0.000000000000000000, 0.000000000000000000 ) ) ;
#1046=AXIS2_PLACEMENT_3D ( 'NONE', #5157, #5053, #4000 ) ;
#1059=DIRECTION ( 'NONE',  ( 0.000000000000000000, 0.000000000000000000, -1.000000000000000000 ) ) ;
#1065=CARTESIAN_POINT ( 'NONE',  ( -0.2277608394786177770, 0.000000000000000000, 12.77499999999999858 ) ) ;
#1067=LINE ( 'NONE', #2613, #3000 ) ;
#1071=ORIENTED_EDGE ( 'NONE', *, *, #778, .F. ) ;
#1086=PLANE ( 'NONE',  #3101 ) ;
#1109=AXIS2_PLACEMENT_3D ( 'NONE', #6519, #7075, #1923 ) ;
#1122=CIRCLE ( 'NONE', #2298, 12.44999999999999929 ) ;
#1142=VERTEX_POINT ( 'NONE', #1707 ) ;
#1143=VECTOR ( 'NONE', #545, 1000.000000000000000 ) ;
#1151=EDGE_CURVE ( 'NONE', #2749, #1904, #6663, .T. ) ;
#1161=EDGE_LOOP ( 'NONE', ( #6055, #3583, #7024, #1945 ) ) ;
#1170=ORIENTED_EDGE ( 'NONE', *, *, #2359, .T. ) ;
#1187=SHAPE_DEFINITION_REPRESENTATION ( #345, #5294 ) ;
#1198=ORIENTED_EDGE ( 'NONE', *, *, #5947, .F. ) ;
#1202=DIRECTION ( 'NONE',  ( 0.000000000000000000, 0.000000000000000000, -1.000000000000000000 ) ) ;
#1209=ORIENTED_EDGE ( 'NONE', *, *, #4502, .F. ) ;
#1231=CARTESIAN_POINT ( 'NONE',  ( -1.800000000000001155, 0.000000000000000000, 0.000000000000000000 ) ) ;
#1239=CIRCLE ( 'NONE', #5300, 9.999999999999994671 ) ;
#1254=ORIENTED_EDGE ( 'NONE', *, *, #4766, .T. ) ;
#1279=EDGE_LOOP ( 'NONE', ( #2472, #3546, #4649, #7331 ) ) ;
#1282=CYLINDRICAL_SURFACE ( 'NONE', #4577, 9.999999999999996447 ) ;
#1295=EDGE_LOOP ( 'NONE', ( #2418, #3734, #5993, #5762 ) ) ;
#1296=EDGE_CURVE ( 'NONE', #5339, #4696, #2111, .T. ) ;
#1300=ORIENTED_EDGE ( 'NONE', *, *, #4328, .F. ) ;
#1303=CYLINDRICAL_SURFACE ( 'NONE', #6167, 10.72500000000000142 ) ;
#1311=CARTESIAN_POINT ( 'NONE',  ( -0.7826237921249277196, 0.000000000000000000, 0.000000000000000000 ) ) ;
#1312=FACE_OUTER_BOUND ( 'NONE', #6458, .T. ) ;
#1321=EDGE_CURVE ( 'NONE', #5898, #3234, #1480, .T. ) ;
#1344=VERTEX_POINT ( 'NONE', #5480 ) ;
#1359=AXIS2_PLACEMENT_3D ( 'NONE', #2120, #6070, #1445 ) ;
#1371=PLANE ( 'NONE',  #5056 ) ;
#1372=DIRECTION ( 'NONE',  ( 0.000000000000000000, 0.000000000000000000, -1.000000000000000000 ) ) ;
#1381=DIRECTION ( 'NONE',  ( 0.000000000000000000, 0.000000000000000000, -1.000000000000000000 ) ) ;
#1392=DIRECTION ( 'NONE',  ( 0.000000000000000000, 1.000000000000000000, -1.224646799147353207E-16 ) ) ;
#1400=EDGE_LOOP ( 'NONE', ( #2, #490, #6515, #775 ) ) ;
#1401=DIRECTION ( 'NONE',  ( 0.000000000000000000, 0.000000000000000000, -1.000000000000000000 ) ) ;
#1405=ORIENTED_EDGE ( 'NONE', *, *, #2918, .F. ) ;
#1407=DIRECTION ( 'NONE',  ( 0.000000000000000000, 0.000000000000000000, 1.000000000000000000 ) ) ;
#1410=ADVANCED_FACE ( 'NONE', ( #1005 ), #2214, .T. ) ;
#1415=DIRECTION ( 'NONE',  ( 0.000000000000000000, 0.000000000000000000, -1.000000000000000000 ) ) ;
#1425=DIRECTION ( 'NONE',  ( 0.000000000000000000, 1.224646799147351975E-16, 1.000000000000000000 ) ) ;
#1427=DIRECTION ( 'NONE',  ( 0.000000000000000000, 0.000000000000000000, -1.000000000000000000 ) ) ;
#1429=CYLINDRICAL_SURFACE ( 'NONE', #2535, 13.50000000000000355 ) ;
#1445=DIRECTION ( 'NONE',  ( 0.000000000000000000, 0.000000000000000000, -1.000000000000000000 ) ) ;
#1460=LINE ( 'NONE', #6200, #3483 ) ;
#1480=LINE ( 'NONE', #1954, #5208 ) ;
#1509=CARTESIAN_POINT ( 'NONE',  ( 0.000000000000000000, 0.000000000000000000, 11.75000000000000000 ) ) ;
#1512=DIRECTION ( 'NONE',  ( -1.000000000000000000, -0.000000000000000000, -0.000000000000000000 ) ) ;
#1514=CIRCLE ( 'NONE', #5449, 10.72500000000000142 ) ;
#1519=AXIS2_PLACEMENT_3D ( 'NONE', #3177, #2023, #2070 ) ;
#1530=DIRECTION ( 'NONE',  ( -1.000000000000000000, -0.000000000000000000, -0.000000000000000000 ) ) ;
#1541=ORIENTED_EDGE ( 'NONE', *, *, #6416, .T. ) ;
#1545=CARTESIAN_POINT ( 'NONE',  ( 1.800000000000002931, 1.653273178848927261E-15, 13.50000000000000178 ) ) ;
#1546=CARTESIAN_POINT ( 'NONE',  ( 2.000000000000001776, 1.641026710857453312E-15, 13.29999999999999893 ) ) ;
#1563=VERTEX_POINT ( 'NONE', #1628 ) ;
#1595=CIRCLE ( 'NONE', #4586, 0.2000000000000022593 ) ;
#1607=AXIS2_PLACEMENT_3D ( 'NONE', #5888, #4687, #5358 ) ;
#1621=CARTESIAN_POINT ( 'NONE',  ( -20.63749999999999574, 0.000000000000000000, -12.44999999999999929 ) ) ;
#1628=CARTESIAN_POINT ( 'NONE',  ( 1.799999999999996048, 1.236893267138826416E-15, 9.999999999999994671 ) ) ;
#1629=DIRECTION ( 'NONE',  ( -0.000000000000000000, 0.000000000000000000, 1.000000000000000000 ) ) ;
#1631=AXIS2_PLACEMENT_3D ( 'NONE', #5110, #4074, #120 ) ;
#1645=FACE_OUTER_BOUND ( 'NONE', #6486, .T. ) ;
#1660=CARTESIAN_POINT ( 'NONE',  ( -1.999999999999998224, 0.000000000000000000, 0.000000000000000000 ) ) ;
#1668=ORIENTED_EDGE ( 'NONE', *, *, #778, .T. ) ;
#1671=CARTESIAN_POINT ( 'NONE',  ( -1.800000000000001155, 0.000000000000000000, 0.000000000000000000 ) ) ;
#1678=CYLINDRICAL_SURFACE ( 'NONE', #3640, 12.77499999999999858 ) ;
#1689=CARTESIAN_POINT ( 'NONE',  ( -20.63749999999999929, 0.000000000000000000, -9.999999999999996447 ) ) ;
#1692=DIRECTION ( 'NONE',  ( 1.000000000000000000, 0.000000000000000000, 0.000000000000000000 ) ) ;
#1702=ORIENTED_EDGE ( 'NONE', *, *, #6260, .T. ) ;
#1707=CARTESIAN_POINT ( 'NONE',  ( -1.799999999999996048, 0.000000000000000000, -9.999999999999998224 ) ) ;
#1715=CIRCLE ( 'NONE', #437, 1.050000000000000488 ) ;
#1716=CLOSED_SHELL ( 'NONE', ( #378, #6599, #1410, #865, #6050, #2554, #4984, #5391, #6299, #6148, #5424, #3936, #602, #6504, #3955, #3007, #4029, #3482, #2873, #132, #2862, #187, #6918, #5243, #567, #2597, #5636, #4148 ) ) ;
#1721=AXIS2_PLACEMENT_3D ( 'NONE', #6193, #7200, #2056 ) ;
#1738=CARTESIAN_POINT ( 'NONE',  ( 1.999999999999994893, 0.000000000000000000, 0.000000000000000000 ) ) ;
#1739=AXIS2_PLACEMENT_3D ( 'NONE', #3605, #4103, #5761 ) ;
#1750=ORIENTED_EDGE ( 'NONE', *, *, #3332, .F. ) ;
#1759=DIRECTION ( 'NONE',  ( 1.000000000000000000, 0.000000000000000000, 0.000000000000000000 ) ) ;
#1763=EDGE_LOOP ( 'NONE', ( #5244, #4423 ) ) ;
#1774=EDGE_CURVE ( 'NONE', #5766, #380, #5098, .T. ) ;
#1788=CARTESIAN_POINT ( 'NONE',  ( -20.63749999999999929, 0.000000000000000000, 0.000000000000000000 ) ) ;
#1790=CARTESIAN_POINT ( 'NONE',  ( 0.000000000000000000, 0.000000000000000000, 0.000000000000000000 ) ) ;
#1791=ORIENTED_EDGE ( 'NONE', *, *, #5133, .T. ) ;
#1807=EDGE_LOOP ( 'NONE', ( #1198, #3974, #6007, #523 ) ) ;
#1813=CARTESIAN_POINT ( 'NONE',  ( -1.800000000000002931, 0.000000000000000000, 0.000000000000000000 ) ) ;
#1816=EDGE_CURVE ( 'NONE', #478, #2671, #4506, .T. ) ;
#1819=DIRECTION ( 'NONE',  ( 0.000000000000000000, 0.000000000000000000, -1.000000000000000000 ) ) ;
#1834=COLOUR_RGB ( '',1.000000000000000000, 0.9490196078431372140, 0.9098039215686274384 ) ;
#1841=ORIENTED_EDGE ( 'NONE', *, *, #2351, .T. ) ;
#1855=DIRECTION ( 'NONE',  ( 0.000000000000000000, 0.000000000000000000, -1.000000000000000000 ) ) ;
#1863=DIRECTION ( 'NONE',  ( -1.000000000000000000, -0.000000000000000000, -0.000000000000000000 ) ) ;
#1870=DIRECTION ( 'NONE',  ( 0.000000000000000000, 0.000000000000000000, -1.000000000000000000 ) ) ;
#1888=DIRECTION ( 'NONE',  ( 1.000000000000000000, 0.000000000000000000, 0.000000000000000000 ) ) ;
#1897=CARTESIAN_POINT ( 'NONE',  ( -1.999999999999998224, 0.000000000000000000, 0.000000000000000000 ) ) ;
#1901=EDGE_CURVE ( 'NONE', #2671, #2792, #5213, .T. ) ;
#1904=VERTEX_POINT ( 'NONE', #5622 ) ;
#1923=DIRECTION ( 'NONE',  ( 0.000000000000000000, 0.000000000000000000, 1.000000000000000000 ) ) ;
#1937=CARTESIAN_POINT ( 'NONE',  ( 1.799999999999996048, 1.249139735130300365E-15, 10.20000000000000107 ) ) ;
#1945=ORIENTED_EDGE ( 'NONE', *, *, #5712, .F. ) ;
#1946=CIRCLE ( 'NONE', #5557, 10.20000000000000107 ) ;
#1954=CARTESIAN_POINT ( 'NONE',  ( -20.63749999999999929, 0.000000000000000000, -11.05000000000000071 ) ) ;
#1955=EDGE_CURVE ( 'NONE', #1344, #6275, #2443, .T. ) ;
#1963=AXIS2_PLACEMENT_3D ( 'NONE', #2294, #628, #5829 ) ;
#1978=DIRECTION ( 'NONE',  ( 0.000000000000000000, -1.224646799147352468E-16, 1.000000000000000000 ) ) ;
#1992=CARTESIAN_POINT ( 'NONE',  ( 1.799999999999996048, 0.000000000000000000, 0.000000000000000000 ) ) ;
#1997=CARTESIAN_POINT ( 'NONE',  ( 0.2277608394786177770, 0.000000000000000000, 10.72500000000000142 ) ) ;
#2000=DIRECTION ( 'NONE',  ( 0.000000000000000000, 0.000000000000000000, -1.000000000000000000 ) ) ;
#2014=FACE_OUTER_BOUND ( 'NONE', #5398, .T. ) ;
#2015=ORIENTED_EDGE ( 'NONE', *, *, #6750, .T. ) ;
#2023=DIRECTION ( 'NONE',  ( 1.000000000000000000, 0.000000000000000000, 0.000000000000000000 ) ) ;
#2026=ORIENTED_EDGE ( 'NONE', *, *, #2351, .F. ) ;
#2047=ORIENTED_EDGE ( 'NONE', *, *, #3451, .T. ) ;
#2052=FACE_OUTER_BOUND ( 'NONE', #2116, .T. ) ;
#2055=CARTESIAN_POINT ( 'NONE',  ( 0.000000000000000000, 0.000000000000000000, 0.000000000000000000 ) ) ;
#2056=DIRECTION ( 'NONE',  ( 0.000000000000000000, 0.000000000000000000, 1.000000000000000000 ) ) ;
#2063=TOROIDAL_SURFACE ( 'NONE', #5413, 13.29999999999999893, 0.2000000000000027034 ) ;
#2070=DIRECTION ( 'NONE',  ( 0.000000000000000000, 0.000000000000000000, -1.000000000000000000 ) ) ;
#2080=UNCERTAINTY_MEASURE_WITH_UNIT (LENGTH_MEASURE( 1.000000000000000082E-05 ), #4291, 'distance_accuracy_value', 'NONE');
#2081=EDGE_LOOP ( 'NONE', ( #1750, #4190 ) ) ;
#2088=CIRCLE ( 'NONE', #1739, 9.999999999999998224 ) ;
#2096=AXIS2_PLACEMENT_3D ( 'NONE', #4829, #6529, #1425 ) ;
#2100=CYLINDRICAL_SURFACE ( 'NONE', #6885, 11.05000000000000071 ) ;
#2102=DIRECTION ( 'NONE',  ( 1.000000000000000000, 0.000000000000000000, 0.000000000000000000 ) ) ;
#2107=CARTESIAN_POINT ( 'NONE',  ( 2.000000000000001776, 0.000000000000000000, -12.44999999999999929 ) ) ;
#2111=CIRCLE ( 'NONE', #1519, 10.20000000000000107 ) ;
#2116=EDGE_LOOP ( 'NONE', ( #6231, #3523, #3692, #7111 ) ) ;
#2120=CARTESIAN_POINT ( 'NONE',  ( -1.799999999999996048, 0.000000000000000000, 0.000000000000000000 ) ) ;
#2129=CARTESIAN_POINT ( 'NONE',  ( -1.799999999999996048, 0.000000000000000000, -10.20000000000000107 ) ) ;
#2140=EDGE_CURVE ( 'NONE', #5732, #2792, #6873, .T. ) ;
#2144=DIRECTION ( 'NONE',  ( 0.000000000000000000, 1.224646799147361589E-16, 1.000000000000000000 ) ) ;
#2178=DIRECTION ( 'NONE',  ( 0.000000000000000000, 0.000000000000000000, -1.000000000000000000 ) ) ;
#2200=ORIENTED_EDGE ( 'NONE', *, *, #361, .T. ) ;
#2211=FACE_OUTER_BOUND ( 'NONE', #6930, .T. ) ;
#2214=TOROIDAL_SURFACE ( 'NONE', #6778, 13.29999999999999893, 0.2000000000000027034 ) ;
#2229=DIRECTION ( 'NONE',  ( 1.000000000000000000, 0.000000000000000000, 0.000000000000000000 ) ) ;
#2253=CARTESIAN_POINT ( 'NONE',  ( 1.999999999999998224, 0.000000000000000000, 0.000000000000000000 ) ) ;
#2278=CIRCLE ( 'NONE', #33, 13.29999999999999893 ) ;
#2281=EDGE_CURVE ( 'NONE', #3012, #1563, #1239, .T. ) ;
#2294=CARTESIAN_POINT ( 'NONE',  ( 0.000000000000000000, 0.000000000000000000, 0.000000000000000000 ) ) ;
#2298=AXIS2_PLACEMENT_3D ( 'NONE', #2537, #2391, #1870 ) ;
#2348=( NAMED_UNIT ( * ) SI_UNIT ( $, .STERADIAN. ) SOLID_ANGLE_UNIT ( ) );
#2350=FACE_OUTER_BOUND ( 'NONE', #3307, .T. ) ;
#2351=EDGE_CURVE ( 'NONE', #6365, #3602, #7218, .T. ) ;
#2359=EDGE_CURVE ( 'NONE', #918, #5828, #1715, .T. ) ;
#2371=CYLINDRICAL_SURFACE ( 'NONE', #4140, 12.77499999999999858 ) ;
#2391=DIRECTION ( 'NONE',  ( 1.000000000000000000, 0.000000000000000000, 0.000000000000000000 ) ) ;
#2395=ORIENTED_EDGE ( 'NONE', *, *, #5314, .F. ) ;
#2404=TOROIDAL_SURFACE ( 'NONE', #6615, 11.75000000000000000, 1.050000000000000266 ) ;
#2418=ORIENTED_EDGE ( 'NONE', *, *, #5722, .F. ) ;
#2432=AXIS2_PLACEMENT_3D ( 'NONE', #5696, #5729, #6221 ) ;
#2437=ORIENTED_EDGE ( 'NONE', *, *, #1296, .T. ) ;
#2438=CIRCLE ( 'NONE', #6525, 12.44999999999999929 ) ;
#2443=CIRCLE ( 'NONE', #1631, 13.29999999999999893 ) ;
#2457=ORIENTED_EDGE ( 'NONE', *, *, #4619, .T. ) ;
#2461=ORIENTED_EDGE ( 'NONE', *, *, #395, .T. ) ;
#2472=ORIENTED_EDGE ( 'NONE', *, *, #2628, .F. ) ;
#2509=ORIENTED_EDGE ( 'NONE', *, *, #1774, .T. ) ;
#2526=TOROIDAL_SURFACE ( 'NONE', #2994, 10.20000000000000107, 0.2000000000000031197 ) ;
#2533=DIRECTION ( 'NONE',  ( 0.000000000000000000, 0.000000000000000000, -1.000000000000000000 ) ) ;
#2535=AXIS2_PLACEMENT_3D ( 'NONE', #4237, #6533, #4913 ) ;
#2537=CARTESIAN_POINT ( 'NONE',  ( 2.000000000000001776, 0.000000000000000000, 0.000000000000000000 ) ) ;
#2542=DIRECTION ( 'NONE',  ( -1.000000000000000000, -0.000000000000000000, -0.000000000000000000 ) ) ;
#2554=ADVANCED_FACE ( 'NONE', ( #6601 ), #3495, .T. ) ;
#2556=AXIS2_PLACEMENT_3D ( 'NONE', #6850, #5016, #455 ) ;
#2561=CARTESIAN_POINT ( 'NONE',  ( 1.799999999999996048, 0.000000000000000000, 0.000000000000000000 ) ) ;
#2571=DIRECTION ( 'NONE',  ( 1.000000000000000000, 0.000000000000000000, 0.000000000000000000 ) ) ;
#2581=DIRECTION ( 'NONE',  ( 0.000000000000000000, -1.000000000000000000, 0.000000000000000000 ) ) ;
#2594=DIRECTION ( 'NONE',  ( 1.000000000000000000, 0.000000000000000000, 0.000000000000000000 ) ) ;
#2597=ADVANCED_FACE ( 'NONE', ( #57 ), #3010, .T. ) ;
#2613=CARTESIAN_POINT ( 'NONE',  ( -20.63749999999999929, 0.000000000000000000, -10.72500000000000142 ) ) ;
#2628=EDGE_CURVE ( 'NONE', #3068, #2674, #177, .T. ) ;
#2671=VERTEX_POINT ( 'NONE', #4544 ) ;
#2674=VERTEX_POINT ( 'NONE', #649 ) ;
#2682=ORIENTED_EDGE ( 'NONE', *, *, #4703, .T. ) ;
#2691=EDGE_CURVE ( 'NONE', #4696, #5339, #4597, .T. ) ;
#2714=ORIENTED_EDGE ( 'NONE', *, *, #6878, .F. ) ;
#2715=DIRECTION ( 'NONE',  ( 0.000000000000000000, 0.000000000000000000, -1.000000000000000000 ) ) ;
#2734=DIRECTION ( 'NONE',  ( 0.000000000000000000, 0.000000000000000000, -1.000000000000000000 ) ) ;
#2736=FACE_OUTER_BOUND ( 'NONE', #5972, .T. ) ;
#2747=TOROIDAL_SURFACE ( 'NONE', #7059, 13.29999999999999893, 0.2000000000000027034 ) ;
#2749=VERTEX_POINT ( 'NONE', #2842 ) ;
#2774=DIRECTION ( 'NONE',  ( 0.000000000000000000, 0.000000000000000000, 1.000000000000000000 ) ) ;
#2780=ORIENTED_EDGE ( 'NONE', *, *, #6537, .F. ) ;
#2785=CARTESIAN_POINT ( 'NONE',  ( 1.999999999999997335, 10.20000000000000107, 0.000000000000000000 ) ) ;
#2786=VECTOR ( 'NONE', #3616, 1000.000000000000000 ) ;
#2792=VERTEX_POINT ( 'NONE', #233 ) ;
#2795=STYLED_ITEM ( 'NONE', ( #7327 ), #5044 ) ;
#2811=DIRECTION ( 'NONE',  ( 0.000000000000000000, 0.000000000000000000, -1.000000000000000000 ) ) ;
#2819=ORIENTED_EDGE ( 'NONE', *, *, #638, .T. ) ;
#2842=CARTESIAN_POINT ( 'NONE',  ( 1.999999999999998668, 0.000000000000000000, -10.20000000000000107 ) ) ;
#2862=ADVANCED_FACE ( 'NONE', ( #2350 ), #2404, .T. ) ;
#2872=CARTESIAN_POINT ( 'NONE',  ( 1.800000000000001155, 0.000000000000000000, 0.000000000000000000 ) ) ;
#2873=ADVANCED_FACE ( 'NONE', ( #3577 ), #2526, .T. ) ;
#2878=CARTESIAN_POINT ( 'NONE',  ( -1.999999999999998224, 0.000000000000000000, -11.05000000000000071 ) ) ;
#2894=CIRCLE ( 'NONE', #7106, 0.2000000000000022593 ) ;
#2902=DIRECTION ( 'NONE',  ( 1.000000000000000000, 0.000000000000000000, 0.000000000000000000 ) ) ;
#2905=SURFACE_STYLE_FILL_AREA ( #400 ) ;
#2918=EDGE_CURVE ( 'NONE', #1142, #4696, #1595, .T. ) ;
#2940=EDGE_CURVE ( 'NONE', #478, #5732, #3488, .T. ) ;
#2978=DIRECTION ( 'NONE',  ( 0.000000000000000000, 1.224646799147361589E-16, 1.000000000000000000 ) ) ;
#2988=CIRCLE ( 'NONE', #992, 11.05000000000000071 ) ;
#2994=AXIS2_PLACEMENT_3D ( 'NONE', #3049, #5350, #6589 ) ;
#3000=VECTOR ( 'NONE', #1032, 1000.000000000000000 ) ;
#3002=FACE_OUTER_BOUND ( 'NONE', #1400, .T. ) ;
#3004=CARTESIAN_POINT ( 'NONE',  ( -20.63749999999999929, 0.000000000000000000, 0.000000000000000000 ) ) ;
#3007=ADVANCED_FACE ( 'NONE', ( #3923, #3997 ), #4559, .T. ) ;
#3010=TOROIDAL_SURFACE ( 'NONE', #4956, 13.29999999999999893, 0.2000000000000027034 ) ;
#3012=VERTEX_POINT ( 'NONE', #5514 ) ;
#3028=ORIENTED_EDGE ( 'NONE', *, *, #1955, .F. ) ;
#3029=CIRCLE ( 'NONE', #3277, 9.999999999999994671 ) ;
#3040=DIRECTION ( 'NONE',  ( 1.000000000000000000, 0.000000000000000000, 0.000000000000000000 ) ) ;
#3049=CARTESIAN_POINT ( 'NONE',  ( -1.799999999999996048, 0.000000000000000000, 0.000000000000000000 ) ) ;
#3054=DIRECTION ( 'NONE',  ( -0.000000000000000000, 1.000000000000000000, 1.224646799147353207E-16 ) ) ;
#3067=UNCERTAINTY_MEASURE_WITH_UNIT (LENGTH_MEASURE( 1.000000000000000082E-05 ), #7253, 'distance_accuracy_value', 'NONE');
#3068=VERTEX_POINT ( 'NONE', #923 ) ;
#3081=CARTESIAN_POINT ( 'NONE',  ( -2.000000000000001776, 0.000000000000000000, 0.000000000000000000 ) ) ;
#3097=ORIENTED_EDGE ( 'NONE', *, *, #5133, .F. ) ;
#3099=CARTESIAN_POINT ( 'NONE',  ( -2.000000000000000888, 12.77500000000000036, 0.000000000000000000 ) ) ;
#3101=AXIS2_PLACEMENT_3D ( 'NONE', #5159, #3674, #1401 ) ;
#3104=VERTEX_POINT ( 'NONE', #4882 ) ;
#3113=CIRCLE ( 'NONE', #6560, 0.2000000000000022593 ) ;
#3125=CIRCLE ( 'NONE', #1359, 9.999999999999998224 ) ;
#3133=DIRECTION ( 'NONE',  ( 1.000000000000000000, 0.000000000000000000, 0.000000000000000000 ) ) ;
#3149=DIRECTION ( 'NONE',  ( 0.000000000000000000, 0.000000000000000000, 1.000000000000000000 ) ) ;
#3166=LINE ( 'NONE', #1621, #5540 ) ;
#3177=CARTESIAN_POINT ( 'NONE',  ( -1.999999999999998224, 0.000000000000000000, 0.000000000000000000 ) ) ;
#3202=DIRECTION ( 'NONE',  ( 0.000000000000000000, 0.000000000000000000, -1.000000000000000000 ) ) ;
#3224=DIRECTION ( 'NONE',  ( 0.000000000000000000, -1.000000000000000000, 0.000000000000000000 ) ) ;
#3226=ORIENTED_EDGE ( 'NONE', *, *, #2628, .T. ) ;
#3228=CYLINDRICAL_SURFACE ( 'NONE', #6608, 10.72500000000000142 ) ;
#3234=VERTEX_POINT ( 'NONE', #242 ) ;
#3243=DIRECTION ( 'NONE',  ( 0.000000000000000000, -1.000000000000000000, 0.000000000000000000 ) ) ;
#3277=AXIS2_PLACEMENT_3D ( 'NONE', #1992, #4978, #1372 ) ;
#3291=DIRECTION ( 'NONE',  ( 1.000000000000000000, 0.000000000000000000, 0.000000000000000000 ) ) ;
#3298=CARTESIAN_POINT ( 'NONE',  ( -0.2277608394786177770, 0.000000000000000000, 0.000000000000000000 ) ) ;
#3301=CARTESIAN_POINT ( 'NONE',  ( 0.2277608394786177770, 1.419059478511995659E-15, -10.72500000000000142 ) ) ;
#3302=FILL_AREA_STYLE_COLOUR ( '', #1834 ) ;
#3307=EDGE_LOOP ( 'NONE', ( #1209, #2457, #1702, #2819 ) ) ;
#3321=CARTESIAN_POINT ( 'NONE',  ( -0.7826237921249277196, 0.000000000000000000, 0.000000000000000000 ) ) ;
#3322=EDGE_LOOP ( 'NONE', ( #4825, #5952, #1170, #2682 ) ) ;
#3323=ORIENTED_EDGE ( 'NONE', *, *, #2691, .T. ) ;
#3328=CARTESIAN_POINT ( 'NONE',  ( 1.799999999999996048, 0.000000000000000000, 0.000000000000000000 ) ) ;
#3329=EDGE_CURVE ( 'NONE', #3602, #6275, #3611, .T. ) ;
#3332=EDGE_CURVE ( 'NONE', #4483, #841, #1122, .T. ) ;
#3359=ORIENTED_EDGE ( 'NONE', *, *, #638, .F. ) ;
#3364=DIRECTION ( 'NONE',  ( 0.000000000000000000, 0.000000000000000000, -1.000000000000000000 ) ) ;
#3385=DIRECTION ( 'NONE',  ( 1.000000000000000000, 0.000000000000000000, 0.000000000000000000 ) ) ;
#3389=ORIENTED_EDGE ( 'NONE', *, *, #4516, .F. ) ;
#3391=AXIS2_PLACEMENT_3D ( 'NONE', #6425, #4129, #2533 ) ;
#3393=CIRCLE ( 'NONE', #5911, 11.05000000000000071 ) ;
#3398=AXIS2_PLACEMENT_3D ( 'NONE', #3328, #5143, #3364 ) ;
#3434=DIRECTION ( 'NONE',  ( 1.000000000000000000, 0.000000000000000000, 0.000000000000000000 ) ) ;
#3444=EDGE_LOOP ( 'NONE', ( #1300, #6344, #1541, #6899 ) ) ;
#3448=DIRECTION ( 'NONE',  ( 1.000000000000000000, 0.000000000000000000, 0.000000000000000000 ) ) ;
#3451=EDGE_CURVE ( 'NONE', #3234, #5460, #3731, .T. ) ;
#3482=ADVANCED_FACE ( 'NONE', ( #4233 ), #1282, .F. ) ;
#3483=VECTOR ( 'NONE', #1759, 1000.000000000000000 ) ;
#3488=CIRCLE ( 'NONE', #4466, 13.29999999999999893 ) ;
#3490=ORIENTED_EDGE ( 'NONE', *, *, #484, .T. ) ;
#3493=DIRECTION ( 'NONE',  ( 1.000000000000000000, 0.000000000000000000, 0.000000000000000000 ) ) ;
#3495=TOROIDAL_SURFACE ( 'NONE', #6295, 11.75000000000000000, 1.050000000000000266 ) ;
#3498=DIRECTION ( 'NONE',  ( 0.000000000000000000, 0.000000000000000000, -1.000000000000000000 ) ) ;
#3517=LINE ( 'NONE', #6808, #6122 ) ;
#3520=DIRECTION ( 'NONE',  ( 0.000000000000000000, 1.224646799147351975E-16, 1.000000000000000000 ) ) ;
#3521=EDGE_CURVE ( 'NONE', #5898, #3857, #2988, .T. ) ;
#3523=ORIENTED_EDGE ( 'NONE', *, *, #6537, .T. ) ;
#3527=( GEOMETRIC_REPRESENTATION_CONTEXT ( 3 ) GLOBAL_UNCERTAINTY_ASSIGNED_CONTEXT ( ( #2080 ) ) GLOBAL_UNIT_ASSIGNED_CONTEXT ( ( #4291, #3769, #4853 ) ) REPRESENTATION_CONTEXT ( 'NONE', 'WORKASPACE' ) );
#3546=ORIENTED_EDGE ( 'NONE', *, *, #735, .T. ) ;
#3576=ORIENTED_EDGE ( 'NONE', *, *, #361, .F. ) ;
#3577=FACE_OUTER_BOUND ( 'NONE', #1295, .T. ) ;
#3583=ORIENTED_EDGE ( 'NONE', *, *, #6062, .T. ) ;
#3586=DIRECTION ( 'NONE',  ( 1.000000000000000000, 0.000000000000000000, 0.000000000000000000 ) ) ;
#3601=EDGE_CURVE ( 'NONE', #6365, #1344, #6855, .T. ) ;
#3602=VERTEX_POINT ( 'NONE', #1545 ) ;
#3605=CARTESIAN_POINT ( 'NONE',  ( -1.799999999999996048, 0.000000000000000000, 0.000000000000000000 ) ) ;
#3611=CIRCLE ( 'NONE', #6268, 0.2000000000000022593 ) ;
#3616=DIRECTION ( 'NONE',  ( 1.000000000000000000, 0.000000000000000000, 0.000000000000000000 ) ) ;
#3640=AXIS2_PLACEMENT_3D ( 'NONE', #6147, #3493, #7032 ) ;
#3656=FACE_OUTER_BOUND ( 'NONE', #6134, .T. ) ;
#3672=DIRECTION ( 'NONE',  ( 0.000000000000000000, 0.000000000000000000, -1.000000000000000000 ) ) ;
#3674=DIRECTION ( 'NONE',  ( 1.000000000000000000, 0.000000000000000000, 0.000000000000000000 ) ) ;
#3692=ORIENTED_EDGE ( 'NONE', *, *, #3451, .F. ) ;
#3695=EDGE_CURVE ( 'NONE', #2671, #3602, #1460, .T. ) ;
#3705=AXIS2_PLACEMENT_3D ( 'NONE', #673, #7326, #2178 ) ;
#3708=DIRECTION ( 'NONE',  ( 1.000000000000000000, 0.000000000000000000, 0.000000000000000000 ) ) ;
#3709=VERTEX_POINT ( 'NONE', #1065 ) ;
#3723=CARTESIAN_POINT ( 'NONE',  ( -0.7826237921249277196, 1.353234713057825478E-15, 11.05000000000000071 ) ) ;
#3729=DIRECTION ( 'NONE',  ( 1.000000000000000000, 0.000000000000000000, 0.000000000000000000 ) ) ;
#3731=CIRCLE ( 'NONE', #530, 11.05000000000000071 ) ;
#3734=ORIENTED_EDGE ( 'NONE', *, *, #113, .T. ) ;
#3747=CARTESIAN_POINT ( 'NONE',  ( 1.999999999999994893, 0.000000000000000000, 0.000000000000000000 ) ) ;
#3753=DIRECTION ( 'NONE',  ( 1.000000000000000000, 0.000000000000000000, 0.000000000000000000 ) ) ;
#3769=( NAMED_UNIT ( * ) PLANE_ANGLE_UNIT ( ) SI_UNIT ( $, .RADIAN. ) );
#3786=DIRECTION ( 'NONE',  ( 1.000000000000000000, 0.000000000000000000, 0.000000000000000000 ) ) ;
#3805=FACE_OUTER_BOUND ( 'NONE', #6262, .T. ) ;
#3813=ORIENTED_EDGE ( 'NONE', *, *, #5722, .T. ) ;
#3821=CARTESIAN_POINT ( 'NONE',  ( 1.800000000000001155, 0.000000000000000000, -13.29999999999999893 ) ) ;
#3854=VERTEX_POINT ( 'NONE', #5069 ) ;
#3855=DIRECTION ( 'NONE',  ( 0.000000000000000000, 0.000000000000000000, -1.000000000000000000 ) ) ;
#3857=VERTEX_POINT ( 'NONE', #159 ) ;
#3903=AXIS2_PLACEMENT_3D ( 'NONE', #983, #543, #6159 ) ;
#3917=( LENGTH_UNIT ( ) NAMED_UNIT ( * ) SI_UNIT ( .MILLI., .METRE. ) );
#3919=ORIENTED_EDGE ( 'NONE', *, *, #7182, .T. ) ;
#3923=FACE_OUTER_BOUND ( 'NONE', #6556, .T. ) ;
#3927=DIRECTION ( 'NONE',  ( 0.000000000000000000, 0.000000000000000000, -1.000000000000000000 ) ) ;
#3934=EDGE_LOOP ( 'NONE', ( #4210, #4198, #2047, #6430 ) ) ;
#3936=ADVANCED_FACE ( 'NONE', ( #5347 ), #390, .T. ) ;
#3938=ORIENTED_EDGE ( 'NONE', *, *, #3695, .T. ) ;
#3939=CARTESIAN_POINT ( 'NONE',  ( -20.63749999999999574, 0.000000000000000000, -13.50000000000000355 ) ) ;
#3955=ADVANCED_FACE ( 'NONE', ( #3656 ), #744, .T. ) ;
#3961=DIRECTION ( 'NONE',  ( 0.000000000000000000, 0.000000000000000000, -1.000000000000000000 ) ) ;
#3974=ORIENTED_EDGE ( 'NONE', *, *, #5933, .T. ) ;
#3983=CARTESIAN_POINT ( 'NONE',  ( -1.999999999999998668, 0.000000000000000000, -10.20000000000000107 ) ) ;
#3986=DIRECTION ( 'NONE',  ( 0.000000000000000000, 0.000000000000000000, -1.000000000000000000 ) ) ;
#3997=FACE_BOUND ( 'NONE', #6756, .T. ) ;
#3998=PRODUCT_DEFINITION_FORMATION_WITH_SPECIFIED_SOURCE ( 'ANY', '', #870, .NOT_KNOWN. ) ;
#4000=DIRECTION ( 'NONE',  ( 0.000000000000000000, 0.000000000000000000, -1.000000000000000000 ) ) ;
#4020=DIRECTION ( 'NONE',  ( 0.000000000000000000, 0.000000000000000000, -1.000000000000000000 ) ) ;
#4022=ORIENTED_EDGE ( 'NONE', *, *, #735, .F. ) ;
#4029=ADVANCED_FACE ( 'NONE', ( #896 ), #154, .T. ) ;
#4034=ORIENTED_EDGE ( 'NONE', *, *, #746, .F. ) ;
#4036=ORIENTED_EDGE ( 'NONE', *, *, #5712, .T. ) ;
#4044=CARTESIAN_POINT ( 'NONE',  ( -20.63749999999999574, 0.000000000000000000, -12.77499999999999858 ) ) ;
#4047=DIRECTION ( 'NONE',  ( 1.000000000000000000, 0.000000000000000000, 0.000000000000000000 ) ) ;
#4061=ORIENTED_EDGE ( 'NONE', *, *, #1321, .T. ) ;
#4074=DIRECTION ( 'NONE',  ( 1.000000000000000000, 0.000000000000000000, 0.000000000000000000 ) ) ;
#4103=DIRECTION ( 'NONE',  ( 1.000000000000000000, 0.000000000000000000, 0.000000000000000000 ) ) ;
#4122=EDGE_CURVE ( 'NONE', #380, #5828, #855, .T. ) ;
#4129=DIRECTION ( 'NONE',  ( 1.000000000000000000, 0.000000000000000000, 0.000000000000000000 ) ) ;
#4140=AXIS2_PLACEMENT_3D ( 'NONE', #415, #5373, #6142 ) ;
#4147=DIRECTION ( 'NONE',  ( 1.000000000000000000, 0.000000000000000000, 0.000000000000000000 ) ) ;
#4148=ADVANCED_FACE ( 'NONE', ( #6771, #6209 ), #1371, .T. ) ;
#4154=DIRECTION ( 'NONE',  ( 0.000000000000000000, 0.000000000000000000, 1.000000000000000000 ) ) ;
#4161=CARTESIAN_POINT ( 'NONE',  ( -20.63749999999999929, 0.000000000000000000, 0.000000000000000000 ) ) ;
#4180=LINE ( 'NONE', #6479, #2786 ) ;
#4190=ORIENTED_EDGE ( 'NONE', *, *, #7182, .F. ) ;
#4191=DIRECTION ( 'NONE',  ( 1.000000000000000000, 0.000000000000000000, 0.000000000000000000 ) ) ;
#4193=DIRECTION ( 'NONE',  ( 0.000000000000000000, 0.000000000000000000, -1.000000000000000000 ) ) ;
#4198=ORIENTED_EDGE ( 'NONE', *, *, #4502, .T. ) ;
#4210=ORIENTED_EDGE ( 'NONE', *, *, #746, .T. ) ;
#4211=CARTESIAN_POINT ( 'NONE',  ( 0.7826237921249277196, 0.000000000000000000, 0.000000000000000000 ) ) ;
#4215=DIRECTION ( 'NONE',  ( -1.000000000000000000, -0.000000000000000000, -0.000000000000000000 ) ) ;
#4223=CYLINDRICAL_SURFACE ( 'NONE', #4231, 13.50000000000000355 ) ;
#4225=CIRCLE ( 'NONE', #4480, 1.050000000000000488 ) ;
#4231=AXIS2_PLACEMENT_3D ( 'NONE', #6520, #1888, #1381 ) ;
#4233=FACE_OUTER_BOUND ( 'NONE', #3444, .T. ) ;
#4237=CARTESIAN_POINT ( 'NONE',  ( -20.63749999999999574, 0.000000000000000000, 0.000000000000000000 ) ) ;
#4252=APPLICATION_CONTEXT ( 'automotive_design' ) ;
#4270=FACE_OUTER_BOUND ( 'NONE', #5105, .T. ) ;
#4279=DIRECTION ( 'NONE',  ( -0.000000000000000000, 1.000000000000000000, 1.224646799147353207E-16 ) ) ;
#4291=( LENGTH_UNIT ( ) NAMED_UNIT ( * ) SI_UNIT ( .MILLI., .METRE. ) );
#4317=CARTESIAN_POINT ( 'NONE',  ( 0.000000000000000000, 0.000000000000000000, 11.75000000000000000 ) ) ;
#4328=EDGE_CURVE ( 'NONE', #3854, #1563, #3517, .T. ) ;
#4332=CARTESIAN_POINT ( 'NONE',  ( -20.63749999999999929, 0.000000000000000000, 0.000000000000000000 ) ) ;
#4345=EDGE_LOOP ( 'NONE', ( #7014, #7201, #4459, #4759 ) ) ;
#4349=DIRECTION ( 'NONE',  ( 0.000000000000000000, -1.000000000000000000, 0.000000000000000000 ) ) ;
#4350=DIRECTION ( 'NONE',  ( 1.000000000000000000, 0.000000000000000000, 0.000000000000000000 ) ) ;
#4352=CIRCLE ( 'NONE', #7217, 10.72499999999999964 ) ;
#4360=DIRECTION ( 'NONE',  ( 0.000000000000000000, -1.224646799147352468E-16, 1.000000000000000000 ) ) ;
#4376=FACE_OUTER_BOUND ( 'NONE', #1279, .T. ) ;
#4400=CARTESIAN_POINT ( 'NONE',  ( -20.63749999999999574, 1.524685264938454646E-15, 12.44999999999999929 ) ) ;
#4422=DIRECTION ( 'NONE',  ( 0.000000000000000000, -1.000000000000000000, 0.000000000000000000 ) ) ;
#4423=ORIENTED_EDGE ( 'NONE', *, *, #2940, .F. ) ;
#4424=ORIENTED_EDGE ( 'NONE', *, *, #1901, .T. ) ;
#4459=ORIENTED_EDGE ( 'NONE', *, *, #7193, .T. ) ;
#4466=AXIS2_PLACEMENT_3D ( 'NONE', #3081, #3729, #3855 ) ;
#4476=CARTESIAN_POINT ( 'NONE',  ( -1.799999999999996048, 1.249139735130300365E-15, 10.20000000000000107 ) ) ;
#4480=AXIS2_PLACEMENT_3D ( 'NONE', #1509, #3243, #1427 ) ;
#4481=TOROIDAL_SURFACE ( 'NONE', #1721, 11.75000000000000000, 1.050000000000000266 ) ;
#4483=VERTEX_POINT ( 'NONE', #2107 ) ;
#4498=AXIS2_PLACEMENT_3D ( 'NONE', #2785, #3385, #2715 ) ;
#4502=EDGE_CURVE ( 'NONE', #5646, #3234, #137, .T. ) ;
#4504=EDGE_LOOP ( 'NONE', ( #2015, #2509, #5453, #5774 ) ) ;
#4506=CIRCLE ( 'NONE', #2096, 0.2000000000000022593 ) ;
#4510=DIRECTION ( 'NONE',  ( 1.000000000000000000, 0.000000000000000000, 0.000000000000000000 ) ) ;
#4515=ORIENTED_EDGE ( 'NONE', *, *, #5900, .F. ) ;
#4516=EDGE_CURVE ( 'NONE', #5828, #841, #358, .T. ) ;
#4523=ORIENTED_EDGE ( 'NONE', *, *, #1151, .T. ) ;
#4544=CARTESIAN_POINT ( 'NONE',  ( -1.800000000000002931, 1.653273178848927064E-15, 13.50000000000000355 ) ) ;
#4550=DIRECTION ( 'NONE',  ( 1.000000000000000000, 0.000000000000000000, 0.000000000000000000 ) ) ;
#4556=PRODUCT_CONTEXT ( 'NONE', #5129, 'mechanical' ) ;
#4559=PLANE ( 'NONE',  #4498 ) ;
#4569=DIRECTION ( 'NONE',  ( 1.000000000000000000, 0.000000000000000000, 0.000000000000000000 ) ) ;
#4577=AXIS2_PLACEMENT_3D ( 'NONE', #4161, #3586, #753 ) ;
#4586=AXIS2_PLACEMENT_3D ( 'NONE', #2129, #4422, #4824 ) ;
#4597=CIRCLE ( 'NONE', #6629, 10.20000000000000107 ) ;
#4609=AXIS2_PLACEMENT_3D ( 'NONE', #5255, #5790, #3927 ) ;
#4615=LINE ( 'NONE', #4044, #774 ) ;
#4618=DIRECTION ( 'NONE',  ( 1.000000000000000000, 0.000000000000000000, 0.000000000000000000 ) ) ;
#4619=EDGE_CURVE ( 'NONE', #5646, #3709, #4910, .T. ) ;
#4643=CARTESIAN_POINT ( 'NONE',  ( -1.999999999999998668, 1.249139735130300365E-15, 10.20000000000000107 ) ) ;
#4649=ORIENTED_EDGE ( 'NONE', *, *, #4619, .F. ) ;
#4656=ORIENTED_EDGE ( 'NONE', *, *, #5314, .T. ) ;
#4671=CIRCLE ( 'NONE', #6355, 0.2000000000000022593 ) ;
#4684=CARTESIAN_POINT ( 'NONE',  ( -2.000000000000001776, 0.000000000000000000, 0.000000000000000000 ) ) ;
#4687=DIRECTION ( 'NONE',  ( 1.000000000000000000, 0.000000000000000000, 0.000000000000000000 ) ) ;
#4696=VERTEX_POINT ( 'NONE', #3983 ) ;
#4703=EDGE_CURVE ( 'NONE', #5828, #380, #507, .T. ) ;
#4759=ORIENTED_EDGE ( 'NONE', *, *, #6416, .F. ) ;
#4766=EDGE_CURVE ( 'NONE', #5732, #478, #2278, .T. ) ;
#4819=CARTESIAN_POINT ( 'NONE',  ( -20.63749999999999929, 0.000000000000000000, 0.000000000000000000 ) ) ;
#4822=ORIENTED_EDGE ( 'NONE', *, *, #3329, .T. ) ;
#4824=DIRECTION ( 'NONE',  ( 0.000000000000000000, 0.000000000000000000, -1.000000000000000000 ) ) ;
#4825=ORIENTED_EDGE ( 'NONE', *, *, #1774, .F. ) ;
#4829=CARTESIAN_POINT ( 'NONE',  ( -1.800000000000001155, 1.628780242865979758E-15, 13.29999999999999893 ) ) ;
#4852=CYLINDRICAL_SURFACE ( 'NONE', #5299, 12.44999999999999929 ) ;
#4853=( NAMED_UNIT ( * ) SI_UNIT ( $, .STERADIAN. ) SOLID_ANGLE_UNIT ( ) );
#4882=CARTESIAN_POINT ( 'NONE',  ( 1.999999999999994893, 0.000000000000000000, -10.72499999999999964 ) ) ;
#4910=CIRCLE ( 'NONE', #844, 12.77499999999999858 ) ;
#4913=DIRECTION ( 'NONE',  ( 0.000000000000000000, 0.000000000000000000, -1.000000000000000000 ) ) ;
#4928=CARTESIAN_POINT ( 'NONE',  ( 2.000000000000001776, 0.000000000000000000, 0.000000000000000000 ) ) ;
#4948=ORIENTED_EDGE ( 'NONE', *, *, #3695, .F. ) ;
#4956=AXIS2_PLACEMENT_3D ( 'NONE', #2872, #4047, #4020 ) ;
#4966=SURFACE_SIDE_STYLE ('',( #2905 ) ) ;
#4978=DIRECTION ( 'NONE',  ( 1.000000000000000000, 0.000000000000000000, 0.000000000000000000 ) ) ;
#4980=CARTESIAN_POINT ( 'NONE',  ( 0.2277608394786177770, 0.000000000000000000, 0.000000000000000000 ) ) ;
#4984=ADVANCED_FACE ( 'NONE', ( #4270 ), #6468, .T. ) ;
#5007=DIRECTION ( 'NONE',  ( 0.000000000000000000, 1.000000000000000000, -1.224646799147353207E-16 ) ) ;
#5008=( NAMED_UNIT ( * ) SI_UNIT ( $, .STERADIAN. ) SOLID_ANGLE_UNIT ( ) );
#5016=DIRECTION ( 'NONE',  ( 1.000000000000000000, 0.000000000000000000, 0.000000000000000000 ) ) ;
#5017=DIRECTION ( 'NONE',  ( -1.000000000000000000, 0.000000000000000000, -0.000000000000000000 ) ) ;
#5034=DIRECTION ( 'NONE',  ( 0.000000000000000000, 0.000000000000000000, -1.000000000000000000 ) ) ;
#5044=ADVANCED_BREP_SHAPE_REPRESENTATION ( '', ( #856, #1963 ), #5797 ) ;
#5053=DIRECTION ( 'NONE',  ( 1.000000000000000000, 0.000000000000000000, 0.000000000000000000 ) ) ;
#5056=AXIS2_PLACEMENT_3D ( 'NONE', #3099, #5405, #1629 ) ;
#5069=CARTESIAN_POINT ( 'NONE',  ( -1.799999999999996048, 1.224646799147353059E-15, 9.999999999999998224 ) ) ;
#5084=AXIS2_PLACEMENT_3D ( 'NONE', #5409, #5017, #371 ) ;
#5098=CIRCLE ( 'NONE', #77, 1.050000000000000488 ) ;
#5105=EDGE_LOOP ( 'NONE', ( #293, #3813, #5944, #1405 ) ) ;
#5110=CARTESIAN_POINT ( 'NONE',  ( 2.000000000000001776, 0.000000000000000000, 0.000000000000000000 ) ) ;
#5129=APPLICATION_CONTEXT ( 'automotive_design' ) ;
#5133=EDGE_CURVE ( 'NONE', #2792, #6365, #503, .T. ) ;
#5143=DIRECTION ( 'NONE',  ( 1.000000000000000000, 0.000000000000000000, 0.000000000000000000 ) ) ;
#5157=CARTESIAN_POINT ( 'NONE',  ( 1.999999999999998224, 0.000000000000000000, 0.000000000000000000 ) ) ;
#5159=CARTESIAN_POINT ( 'NONE',  ( 2.000000000000001332, 13.29999999999999893, 0.000000000000000000 ) ) ;
#5168=DIRECTION ( 'NONE',  ( 1.000000000000000000, 0.000000000000000000, 0.000000000000000000 ) ) ;
#5190=CIRCLE ( 'NONE', #3391, 13.50000000000000178 ) ;
#5200=ORIENTED_EDGE ( 'NONE', *, *, #6321, .T. ) ;
#5207=DIRECTION ( 'NONE',  ( 0.000000000000000000, 0.000000000000000000, -1.000000000000000000 ) ) ;
#5208=VECTOR ( 'NONE', #959, 1000.000000000000000 ) ;
#5213=CIRCLE ( 'NONE', #3903, 13.50000000000000533 ) ;
#5243=ADVANCED_FACE ( 'NONE', ( #3002 ), #2747, .T. ) ;
#5244=ORIENTED_EDGE ( 'NONE', *, *, #4766, .F. ) ;
#5247=DIRECTION ( 'NONE',  ( 1.000000000000000000, 0.000000000000000000, 0.000000000000000000 ) ) ;
#5255=CARTESIAN_POINT ( 'NONE',  ( -1.800000000000001155, 0.000000000000000000, -13.29999999999999893 ) ) ;
#5270=EDGE_LOOP ( 'NONE', ( #4022, #2714, #5200, #4034 ) ) ;
#5271=AXIS2_PLACEMENT_3D ( 'NONE', #6876, #26, #2774 ) ;
#5294=SHAPE_REPRESENTATION ( 'angular contact ball bearing_68_iso_ISO 15 ABB - 1720 - 28,SI,NC,28_68', ( #1963 ), #5797 ) ;
#5299=AXIS2_PLACEMENT_3D ( 'NONE', #889, #2594, #6141 ) ;
#5300=AXIS2_PLACEMENT_3D ( 'NONE', #7130, #3133, #3672 ) ;
#5307=VERTEX_POINT ( 'NONE', #5310 ) ;
#5309=( GEOMETRIC_REPRESENTATION_CONTEXT ( 3 ) GLOBAL_UNCERTAINTY_ASSIGNED_CONTEXT ( ( #3067 ) ) GLOBAL_UNIT_ASSIGNED_CONTEXT ( ( #7253, #6694, #5008 ) ) REPRESENTATION_CONTEXT ( 'NONE', 'WORKASPACE' ) );
#5310=CARTESIAN_POINT ( 'NONE',  ( 1.999999999999994893, 1.313433692085536476E-15, 10.72499999999999964 ) ) ;
#5311=DIRECTION ( 'NONE',  ( 1.000000000000000000, 0.000000000000000000, 0.000000000000000000 ) ) ;
#5314=EDGE_CURVE ( 'NONE', #918, #5307, #4180, .T. ) ;
#5339=VERTEX_POINT ( 'NONE', #4643 ) ;
#5347=FACE_OUTER_BOUND ( 'NONE', #4504, .T. ) ;
#5348=DIRECTION ( 'NONE',  ( 1.000000000000000000, 0.000000000000000000, 0.000000000000000000 ) ) ;
#5350=DIRECTION ( 'NONE',  ( 1.000000000000000000, 0.000000000000000000, 0.000000000000000000 ) ) ;
#5358=DIRECTION ( 'NONE',  ( 0.000000000000000000, 0.000000000000000000, -1.000000000000000000 ) ) ;
#5373=DIRECTION ( 'NONE',  ( 1.000000000000000000, 0.000000000000000000, 0.000000000000000000 ) ) ;
#5375=DIRECTION ( 'NONE',  ( 1.000000000000000000, 0.000000000000000000, 0.000000000000000000 ) ) ;
#5384=CIRCLE ( 'NONE', #6357, 13.50000000000000533 ) ;
#5391=ADVANCED_FACE ( 'NONE', ( #7146 ), #6672, .F. ) ;
#5397=CARTESIAN_POINT ( 'NONE',  ( 1.800000000000002931, 0.000000000000000000, 0.000000000000000000 ) ) ;
#5398=EDGE_LOOP ( 'NONE', ( #4948, #4424, #1791, #6603 ) ) ;
#5399=AXIS2_PLACEMENT_3D ( 'NONE', #4819, #5375, #1415 ) ;
#5405=DIRECTION ( 'NONE',  ( -1.000000000000000000, 0.000000000000000000, -0.000000000000000000 ) ) ;
#5409=CARTESIAN_POINT ( 'NONE',  ( -1.999999999999996669, 11.05000000000000071, 0.000000000000000000 ) ) ;
#5413=AXIS2_PLACEMENT_3D ( 'NONE', #7318, #3786, #6086 ) ;
#5414=AXIS2_PLACEMENT_3D ( 'NONE', #5397, #3708, #324 ) ;
#5424=ADVANCED_FACE ( 'NONE', ( #971 ), #3228, .T. ) ;
#5448=DIRECTION ( 'NONE',  ( 0.000000000000000000, 0.000000000000000000, -1.000000000000000000 ) ) ;
#5449=AXIS2_PLACEMENT_3D ( 'NONE', #4980, #1530, #3149 ) ;
#5453=ORIENTED_EDGE ( 'NONE', *, *, #4122, .T. ) ;
#5460=VERTEX_POINT ( 'NONE', #3723 ) ;
#5480=CARTESIAN_POINT ( 'NONE',  ( 2.000000000000001776, 0.000000000000000000, -13.29999999999999893 ) ) ;
#5510=CARTESIAN_POINT ( 'NONE',  ( 0.000000000000000000, 1.438959988998140160E-15, -11.75000000000000000 ) ) ;
#5514=CARTESIAN_POINT ( 'NONE',  ( 1.799999999999996048, 0.000000000000000000, -9.999999999999994671 ) ) ;
#5540=VECTOR ( 'NONE', #3291, 1000.000000000000000 ) ;
#5544=ORIENTED_EDGE ( 'NONE', *, *, #329, .F. ) ;
#5554=PRODUCT_DEFINITION_CONTEXT ( 'detailed design', #4252, 'design' ) ;
#5557=AXIS2_PLACEMENT_3D ( 'NONE', #2253, #4550, #3986 ) ;
#5622=CARTESIAN_POINT ( 'NONE',  ( 1.999999999999998668, 1.249139735130300365E-15, 10.20000000000000107 ) ) ;
#5636=ADVANCED_FACE ( 'NONE', ( #1645, #6219 ), #1086, .T. ) ;
#5646=VERTEX_POINT ( 'NONE', #5835 ) ;
#5661=LINE ( 'NONE', #1689, #1143 ) ;
#5686=CIRCLE ( 'NONE', #2432, 10.72500000000000142 ) ;
#5696=CARTESIAN_POINT ( 'NONE',  ( 0.2277608394786177770, 0.000000000000000000, 0.000000000000000000 ) ) ;
#5712=EDGE_CURVE ( 'NONE', #6275, #1344, #6202, .T. ) ;
#5722=EDGE_CURVE ( 'NONE', #3854, #5339, #4671, .T. ) ;
#5729=DIRECTION ( 'NONE',  ( -1.000000000000000000, -0.000000000000000000, -0.000000000000000000 ) ) ;
#5732=VERTEX_POINT ( 'NONE', #482 ) ;
#5761=DIRECTION ( 'NONE',  ( 0.000000000000000000, 0.000000000000000000, -1.000000000000000000 ) ) ;
#5762=ORIENTED_EDGE ( 'NONE', *, *, #1296, .F. ) ;
#5766=VERTEX_POINT ( 'NONE', #3301 ) ;
#5772=SURFACE_STYLE_USAGE ( .BOTH. , #4966 ) ;
#5773=AXIS2_PLACEMENT_3D ( 'NONE', #3821, #4349, #3202 ) ;
#5774=ORIENTED_EDGE ( 'NONE', *, *, #2359, .F. ) ;
#5781=DIRECTION ( 'NONE',  ( 0.000000000000000000, 0.000000000000000000, -1.000000000000000000 ) ) ;
#5790=DIRECTION ( 'NONE',  ( 0.000000000000000000, -1.000000000000000000, 0.000000000000000000 ) ) ;
#5797=( GEOMETRIC_REPRESENTATION_CONTEXT ( 3 ) GLOBAL_UNCERTAINTY_ASSIGNED_CONTEXT ( ( #5943 ) ) GLOBAL_UNIT_ASSIGNED_CONTEXT ( ( #3917, #483, #2348 ) ) REPRESENTATION_CONTEXT ( 'NONE', 'WORKASPACE' ) );
#5828=VERTEX_POINT ( 'NONE', #6609 ) ;
#5829=DIRECTION ( 'NONE',  ( 1.000000000000000000, 0.000000000000000000, 0.000000000000000000 ) ) ;
#5835=CARTESIAN_POINT ( 'NONE',  ( -0.2277608394786177770, 1.564486285910743648E-15, -12.77499999999999858 ) ) ;
#5843=LINE ( 'NONE', #91, #7110 ) ;
#5852=DIRECTION ( 'NONE',  ( 0.000000000000000000, 0.000000000000000000, -1.000000000000000000 ) ) ;
#5871=EDGE_LOOP ( 'NONE', ( #1254, #6664, #1071, #6151 ) ) ;
#5888=CARTESIAN_POINT ( 'NONE',  ( -20.63749999999999574, 0.000000000000000000, 0.000000000000000000 ) ) ;
#5898=VERTEX_POINT ( 'NONE', #2878 ) ;
#5900=EDGE_CURVE ( 'NONE', #5307, #3104, #6990, .T. ) ;
#5911=AXIS2_PLACEMENT_3D ( 'NONE', #3321, #3434, #1059 ) ;
#5933=EDGE_CURVE ( 'NONE', #1904, #2749, #1946, .T. ) ;
#5943=UNCERTAINTY_MEASURE_WITH_UNIT (LENGTH_MEASURE( 1.000000000000000082E-05 ), #3917, 'distance_accuracy_value', 'NONE');
#5944=ORIENTED_EDGE ( 'NONE', *, *, #2691, .F. ) ;
#5947=EDGE_CURVE ( 'NONE', #1904, #1563, #2894, .T. ) ;
#5952=ORIENTED_EDGE ( 'NONE', *, *, #941, .T. ) ;
#5972=EDGE_LOOP ( 'NONE', ( #1841, #4822, #3028, #14 ) ) ;
#5993=ORIENTED_EDGE ( 'NONE', *, *, #2918, .T. ) ;
#6007=ORIENTED_EDGE ( 'NONE', *, *, #175, .T. ) ;
#6009=DIRECTION ( 'NONE',  ( 0.000000000000000000, 0.000000000000000000, -1.000000000000000000 ) ) ;
#6050=ADVANCED_FACE ( 'NONE', ( #1312 ), #7086, .F. ) ;
#6055=ORIENTED_EDGE ( 'NONE', *, *, #3329, .F. ) ;
#6062=EDGE_CURVE ( 'NONE', #3602, #6365, #5190, .T. ) ;
#6070=DIRECTION ( 'NONE',  ( 1.000000000000000000, 0.000000000000000000, 0.000000000000000000 ) ) ;
#6086=DIRECTION ( 'NONE',  ( 0.000000000000000000, 0.000000000000000000, -1.000000000000000000 ) ) ;
#6087=AXIS2_PLACEMENT_3D ( 'NONE', #7242, #2102, #5034 ) ;
#6122=VECTOR ( 'NONE', #6319, 1000.000000000000000 ) ;
#6130=SHAPE_REPRESENTATION_RELATIONSHIP ( 'NONE' , 'NONE' ,  #5294, #5044 ) ;
#6134=EDGE_LOOP ( 'NONE', ( #2780, #2461, #4061, #3359 ) ) ;
#6136=EDGE_LOOP ( 'NONE', ( #3323, #2437 ) ) ;
#6141=DIRECTION ( 'NONE',  ( 0.000000000000000000, 0.000000000000000000, -1.000000000000000000 ) ) ;
#6142=DIRECTION ( 'NONE',  ( 0.000000000000000000, 0.000000000000000000, -1.000000000000000000 ) ) ;
#6147=CARTESIAN_POINT ( 'NONE',  ( -20.63749999999999574, 0.000000000000000000, 0.000000000000000000 ) ) ;
#6148=ADVANCED_FACE ( 'NONE', ( #2052 ), #2100, .T. ) ;
#6151=ORIENTED_EDGE ( 'NONE', *, *, #2140, .F. ) ;
#6159=DIRECTION ( 'NONE',  ( 0.000000000000000000, 0.000000000000000000, -1.000000000000000000 ) ) ;
#6165=DIRECTION ( 'NONE',  ( 0.000000000000000000, 0.000000000000000000, 1.000000000000000000 ) ) ;
#6167=AXIS2_PLACEMENT_3D ( 'NONE', #1788, #2902, #5207 ) ;
#6193=CARTESIAN_POINT ( 'NONE',  ( 0.000000000000000000, 0.000000000000000000, 0.000000000000000000 ) ) ;
#6200=CARTESIAN_POINT ( 'NONE',  ( -20.63749999999999574, 1.653273178848927261E-15, 13.50000000000000355 ) ) ;
#6202=CIRCLE ( 'NONE', #3705, 13.29999999999999893 ) ;
#6206=ORIENTED_EDGE ( 'NONE', *, *, #484, .F. ) ;
#6209=FACE_OUTER_BOUND ( 'NONE', #1763, .T. ) ;
#6219=FACE_BOUND ( 'NONE', #2081, .T. ) ;
#6221=DIRECTION ( 'NONE',  ( 0.000000000000000000, 0.000000000000000000, 1.000000000000000000 ) ) ;
#6226=ORIENTED_EDGE ( 'NONE', *, *, #1955, .T. ) ;
#6231=ORIENTED_EDGE ( 'NONE', *, *, #3521, .T. ) ;
#6259=CARTESIAN_POINT ( 'NONE',  ( -20.63749999999999574, 1.564486285910743648E-15, 12.77499999999999858 ) ) ;
#6260=EDGE_CURVE ( 'NONE', #3709, #5460, #4225, .T. ) ;
#6262=EDGE_LOOP ( 'NONE', ( #3389, #7261, #2200, #6679 ) ) ;
#6268=AXIS2_PLACEMENT_3D ( 'NONE', #833, #278, #3520 ) ;
#6275=VERTEX_POINT ( 'NONE', #1546 ) ;
#6295=AXIS2_PLACEMENT_3D ( 'NONE', #2055, #1512, #6165 ) ;
#6299=ADVANCED_FACE ( 'NONE', ( #2211 ), #887, .T. ) ;
#6315=DIRECTION ( 'NONE',  ( 0.000000000000000000, 0.000000000000000000, -1.000000000000000000 ) ) ;
#6319=DIRECTION ( 'NONE',  ( 1.000000000000000000, 0.000000000000000000, 0.000000000000000000 ) ) ;
#6321=EDGE_CURVE ( 'NONE', #2674, #5646, #4615, .T. ) ;
#6344=ORIENTED_EDGE ( 'NONE', *, *, #6948, .F. ) ;
#6350=ORIENTED_EDGE ( 'NONE', *, *, #2281, .F. ) ;
#6355=AXIS2_PLACEMENT_3D ( 'NONE', #4476, #5007, #2144 ) ;
#6357=AXIS2_PLACEMENT_3D ( 'NONE', #1813, #3040, #3498 ) ;
#6365=VERTEX_POINT ( 'NONE', #506 ) ;
#6366=AXIS2_PLACEMENT_3D ( 'NONE', #2561, #423, #935 ) ;
#6385=PRODUCT_DEFINITION ( 'UNKNOWN', '', #3998, #5554 ) ;
#6396=VECTOR ( 'NONE', #4569, 1000.000000000000000 ) ;
#6411=FACE_OUTER_BOUND ( 'NONE', #7335, .T. ) ;
#6416=EDGE_CURVE ( 'NONE', #1142, #3012, #5661, .T. ) ;
#6425=CARTESIAN_POINT ( 'NONE',  ( 1.800000000000002931, 0.000000000000000000, 0.000000000000000000 ) ) ;
#6426=STYLED_ITEM('',(#7439),#856);
#6430=ORIENTED_EDGE ( 'NONE', *, *, #6260, .F. ) ;
#6440=EDGE_LOOP ( 'NONE', ( #6526, #4656, #6206, #5544 ) ) ;
#6457=DIRECTION ( 'NONE',  ( 0.000000000000000000, 0.000000000000000000, -1.000000000000000000 ) ) ;
#6458=EDGE_LOOP ( 'NONE', ( #827, #46, #3919, #3576 ) ) ;
#6468=TOROIDAL_SURFACE ( 'NONE', #7177, 10.20000000000000107, 0.2000000000000031197 ) ;
#6475=CARTESIAN_POINT ( 'NONE',  ( 2.000000000000001776, 1.524685264938454646E-15, 12.44999999999999929 ) ) ;
#6479=CARTESIAN_POINT ( 'NONE',  ( -20.63749999999999929, 1.313433692085536673E-15, 10.72500000000000142 ) ) ;
#6486=EDGE_LOOP ( 'NONE', ( #6226, #4036 ) ) ;
#6494=DIRECTION ( 'NONE',  ( 1.000000000000000000, 0.000000000000000000, 0.000000000000000000 ) ) ;
#6499=ORIENTED_EDGE ( 'NONE', *, *, #3521, .F. ) ;
#6504=ADVANCED_FACE ( 'NONE', ( #6411 ), #1303, .T. ) ;
#6515=ORIENTED_EDGE ( 'NONE', *, *, #2140, .T. ) ;
#6519=CARTESIAN_POINT ( 'NONE',  ( 0.000000000000000000, 0.000000000000000000, 0.000000000000000000 ) ) ;
#6520=CARTESIAN_POINT ( 'NONE',  ( -20.63749999999999574, 0.000000000000000000, 0.000000000000000000 ) ) ;
#6525=AXIS2_PLACEMENT_3D ( 'NONE', #4928, #7107, #5448 ) ;
#6526=ORIENTED_EDGE ( 'NONE', *, *, #6750, .F. ) ;
#6529=DIRECTION ( 'NONE',  ( 0.000000000000000000, 1.000000000000000000, -1.224646799147353207E-16 ) ) ;
#6533=DIRECTION ( 'NONE',  ( 1.000000000000000000, 0.000000000000000000, 0.000000000000000000 ) ) ;
#6536=ORIENTED_EDGE ( 'NONE', *, *, #5900, .T. ) ;
#6537=EDGE_CURVE ( 'NONE', #3857, #5460, #5843, .T. ) ;
#6556=EDGE_LOOP ( 'NONE', ( #3490, #6536 ) ) ;
#6560=AXIS2_PLACEMENT_3D ( 'NONE', #845, #3224, #6669 ) ;
#6563=CARTESIAN_POINT ( 'NONE',  ( -1.799999999999996048, 0.000000000000000000, 0.000000000000000000 ) ) ;
#6582=EDGE_LOOP ( 'NONE', ( #1668, #3938, #2026, #3097 ) ) ;
#6589=DIRECTION ( 'NONE',  ( 0.000000000000000000, 0.000000000000000000, -1.000000000000000000 ) ) ;
#6599=ADVANCED_FACE ( 'NONE', ( #7041 ), #4223, .T. ) ;
#6601=FACE_OUTER_BOUND ( 'NONE', #3934, .T. ) ;
#6603=ORIENTED_EDGE ( 'NONE', *, *, #6062, .F. ) ;
#6608=AXIS2_PLACEMENT_3D ( 'NONE', #4332, #7184, #2000 ) ;
#6609=CARTESIAN_POINT ( 'NONE',  ( 0.7826237921249276086, 0.000000000000000000, 12.44999999999999929 ) ) ;
#6615=AXIS2_PLACEMENT_3D ( 'NONE', #1790, #1863, #4154 ) ;
#6629=AXIS2_PLACEMENT_3D ( 'NONE', #1660, #4618, #2811 ) ;
#6663=CIRCLE ( 'NONE', #1046, 10.20000000000000107 ) ;
#6664=ORIENTED_EDGE ( 'NONE', *, *, #1816, .T. ) ;
#6669=DIRECTION ( 'NONE',  ( 0.000000000000000000, 0.000000000000000000, -1.000000000000000000 ) ) ;
#6672=CYLINDRICAL_SURFACE ( 'NONE', #5399, 9.999999999999996447 ) ;
#6679=ORIENTED_EDGE ( 'NONE', *, *, #3332, .T. ) ;
#6694=( NAMED_UNIT ( * ) PLANE_ANGLE_UNIT ( ) SI_UNIT ( $, .RADIAN. ) );
#6733=AXIS2_PLACEMENT_3D ( 'NONE', #4211, #253, #1407 ) ;
#6742=PLANE ( 'NONE',  #5084 ) ;
#6750=EDGE_CURVE ( 'NONE', #918, #5766, #5686, .T. ) ;
#6756=EDGE_LOOP ( 'NONE', ( #592, #284 ) ) ;
#6768=MECHANICAL_DESIGN_GEOMETRIC_PRESENTATION_REPRESENTATION('',(#2795),#5309);
#6771=FACE_BOUND ( 'NONE', #943, .T. ) ;
#6778=AXIS2_PLACEMENT_3D ( 'NONE', #1671, #2229, #3961 ) ;
#6808=CARTESIAN_POINT ( 'NONE',  ( -20.63749999999999929, 1.224646799147352862E-15, 9.999999999999996447 ) ) ;
#6823=FACE_OUTER_BOUND ( 'NONE', #5270, .T. ) ;
#6850=CARTESIAN_POINT ( 'NONE',  ( -2.000000000000001776, 0.000000000000000000, 0.000000000000000000 ) ) ;
#6855=CIRCLE ( 'NONE', #5773, 0.2000000000000022593 ) ;
#6871=CARTESIAN_POINT ( 'NONE',  ( -2.000000000000001776, 0.000000000000000000, 0.000000000000000000 ) ) ;
#6873=CIRCLE ( 'NONE', #4609, 0.2000000000000022593 ) ;
#6876=CARTESIAN_POINT ( 'NONE',  ( 0.7826237921249277196, 0.000000000000000000, 0.000000000000000000 ) ) ;
#6878=EDGE_CURVE ( 'NONE', #2674, #3068, #311, .T. ) ;
#6885=AXIS2_PLACEMENT_3D ( 'NONE', #353, #4350, #2734 ) ;
#6899=ORIENTED_EDGE ( 'NONE', *, *, #2281, .T. ) ;
#6918=ADVANCED_FACE ( 'NONE', ( #6823 ), #1678, .F. ) ;
#6929=CARTESIAN_POINT ( 'NONE',  ( -0.2277608394786177770, 0.000000000000000000, 0.000000000000000000 ) ) ;
#6930=EDGE_LOOP ( 'NONE', ( #4523, #7171, #6350, #750 ) ) ;
#6948=EDGE_CURVE ( 'NONE', #1142, #3854, #2088, .T. ) ;
#6975=DIRECTION ( 'NONE',  ( 1.000000000000000000, 0.000000000000000000, 0.000000000000000000 ) ) ;
#6990=CIRCLE ( 'NONE', #770, 10.72499999999999964 ) ;
#7014=ORIENTED_EDGE ( 'NONE', *, *, #113, .F. ) ;
#7024=ORIENTED_EDGE ( 'NONE', *, *, #3601, .T. ) ;
#7032=DIRECTION ( 'NONE',  ( 0.000000000000000000, 0.000000000000000000, -1.000000000000000000 ) ) ;
#7041=FACE_OUTER_BOUND ( 'NONE', #6582, .T. ) ;
#7044=ORIENTED_EDGE ( 'NONE', *, *, #6878, .T. ) ;
#7059=AXIS2_PLACEMENT_3D ( 'NONE', #1231, #4147, #1202 ) ;
#7075=DIRECTION ( 'NONE',  ( -1.000000000000000000, -0.000000000000000000, -0.000000000000000000 ) ) ;
#7079=AXIS2_PLACEMENT_3D ( 'NONE', #3004, #5311, #1819 ) ;
#7086=CYLINDRICAL_SURFACE ( 'NONE', #1607, 12.44999999999999929 ) ;
#7106=AXIS2_PLACEMENT_3D ( 'NONE', #1937, #1392, #2978 ) ;
#7107=DIRECTION ( 'NONE',  ( 1.000000000000000000, 0.000000000000000000, 0.000000000000000000 ) ) ;
#7108=CIRCLE ( 'NONE', #657, 12.77499999999999858 ) ;
#7110=VECTOR ( 'NONE', #5348, 1000.000000000000000 ) ;
#7111=ORIENTED_EDGE ( 'NONE', *, *, #1321, .F. ) ;
#7130=CARTESIAN_POINT ( 'NONE',  ( 1.799999999999996048, 0.000000000000000000, 0.000000000000000000 ) ) ;
#7146=FACE_OUTER_BOUND ( 'NONE', #4345, .T. ) ;
#7156=DIRECTION ( 'NONE',  ( 0.000000000000000000, 0.000000000000000000, -1.000000000000000000 ) ) ;
#7166=ORIENTED_EDGE ( 'NONE', *, *, #395, .F. ) ;
#7171=ORIENTED_EDGE ( 'NONE', *, *, #5947, .T. ) ;
#7177=AXIS2_PLACEMENT_3D ( 'NONE', #6563, #2571, #7156 ) ;
#7182=EDGE_CURVE ( 'NONE', #841, #4483, #2438, .T. ) ;
#7184=DIRECTION ( 'NONE',  ( 1.000000000000000000, 0.000000000000000000, 0.000000000000000000 ) ) ;
#7193=EDGE_CURVE ( 'NONE', #1563, #3012, #3029, .T. ) ;
#7200=DIRECTION ( 'NONE',  ( -1.000000000000000000, -0.000000000000000000, -0.000000000000000000 ) ) ;
#7201=ORIENTED_EDGE ( 'NONE', *, *, #4328, .T. ) ;
#7217=AXIS2_PLACEMENT_3D ( 'NONE', #3747, #6494, #6457 ) ;
#7218=CIRCLE ( 'NONE', #5414, 13.50000000000000178 ) ;
#7242=CARTESIAN_POINT ( 'NONE',  ( -1.999999999999998224, 0.000000000000000000, 0.000000000000000000 ) ) ;
#7253=( LENGTH_UNIT ( ) NAMED_UNIT ( * ) SI_UNIT ( .MILLI., .METRE. ) );
#7261=ORIENTED_EDGE ( 'NONE', *, *, #4122, .F. ) ;
#7318=CARTESIAN_POINT ( 'NONE',  ( 1.800000000000001155, 0.000000000000000000, 0.000000000000000000 ) ) ;
#7326=DIRECTION ( 'NONE',  ( 1.000000000000000000, 0.000000000000000000, 0.000000000000000000 ) ) ;
#7327=PRESENTATION_STYLE_ASSIGNMENT (( #5772 ) ) ;
#7331=ORIENTED_EDGE ( 'NONE', *, *, #6321, .F. ) ;
#7335=EDGE_LOOP ( 'NONE', ( #2395, #408, #700, #4515 ) ) ;
#7433=COLOUR_RGB('Grey',0.48,0.52,0.57);
#7434=FILL_AREA_STYLE_COLOUR('',#7433);
#7435=FILL_AREA_STYLE('',(#7434));
#7436=SURFACE_STYLE_FILL_AREA(#7435);
#7437=SURFACE_SIDE_STYLE('',(#7436));
#7438=SURFACE_STYLE_USAGE(.BOTH.,#7437);
#7439=PRESENTATION_STYLE_ASSIGNMENT((#7438));
ENDSEC;
END-ISO-10303-21;
